ISO-10303-21;
HEADER;
/* Generated by software containing ST-Developer
 * from STEP Tools, Inc. (www.steptools.com) 
 */

FILE_DESCRIPTION(
/* description */ (''),
/* implementation_level */ '2;1');

FILE_NAME(
/* name */ 'Bottom_Block_02.step',
/* time_stamp */ '2026-10-23T22:30:33+06:00',
/* author */ (''),
/* organization */ (''),
/* preprocessor_version */ 'ST-DEVELOPER v20.2',
/* originating_system */ 'Autodesk Translation Framework v15.15.0.0',
/* authorisation */ '');

FILE_SCHEMA (('AUTOMOTIVE_DESIGN { 1 0 10303 214 3 1 1 }'));
ENDSEC;

DATA;
#10=MECHANICAL_DESIGN_GEOMETRIC_PRESENTATION_REPRESENTATION('',(#244),#10131);
#183=ELLIPSE('',#6551,1.08239220029239,1.);
#184=ELLIPSE('',#6552,1.08239220029239,1.);
#185=ELLIPSE('',#6554,1.08239220029239,1.);
#186=ELLIPSE('',#6555,1.08239220029239,1.);
#187=ELLIPSE('',#6557,1.08239220029239,1.);
#188=ELLIPSE('',#6559,1.0823922002924,1.);
#189=ELLIPSE('',#6561,1.08239220029239,1.);
#190=ELLIPSE('',#6563,1.0823922002924,1.);
#191=ELLIPSE('',#6565,1.08239220029239,1.);
#192=ELLIPSE('',#6567,1.0823922002924,1.);
#193=ELLIPSE('',#6569,1.08239220029239,1.);
#194=ELLIPSE('',#6571,1.0823922002924,1.);
#195=ELLIPSE('',#6582,1.08239220029239,1.);
#196=ELLIPSE('',#6583,1.0823922002924,1.);
#197=ELLIPSE('',#6585,1.08239220029239,1.);
#198=ELLIPSE('',#6587,1.0823922002924,1.);
#199=ELLIPSE('',#6589,1.08239220029239,1.);
#200=ELLIPSE('',#6591,1.0823922002924,1.);
#201=ELLIPSE('',#6593,1.08239220029239,1.);
#202=ELLIPSE('',#6595,1.0823922002924,1.);
#203=ELLIPSE('',#6597,1.08239220029239,1.);
#204=ELLIPSE('',#6599,1.0823922002924,1.);
#205=ELLIPSE('',#6601,1.08239220029239,1.);
#206=ELLIPSE('',#6603,1.08239220029239,1.);
#224=SHAPE_REPRESENTATION_RELATIONSHIP('SRR','None',#10178,#234);
#234=ADVANCED_BREP_SHAPE_REPRESENTATION('',(#254),#10130);
#244=STYLED_ITEM('',(#10247),#254);
#254=MANIFOLD_SOLID_BREP('Bottom_Block_02',#5888);
#453=PLANE('',#6574);
#454=PLANE('',#6575);
#455=PLANE('',#6576);
#456=PLANE('',#6577);
#457=PLANE('',#6578);
#458=PLANE('',#6579);
#459=PLANE('',#6580);
#460=PLANE('',#6605);
#461=PLANE('',#6606);
#462=PLANE('',#6607);
#463=PLANE('',#6608);
#464=PLANE('',#6609);
#465=PLANE('',#6610);
#466=PLANE('',#6611);
#778=FACE_OUTER_BOUND('',#1196,.T.);
#779=FACE_OUTER_BOUND('',#1197,.T.);
#780=FACE_OUTER_BOUND('',#1198,.T.);
#781=FACE_OUTER_BOUND('',#1199,.T.);
#782=FACE_OUTER_BOUND('',#1200,.T.);
#783=FACE_OUTER_BOUND('',#1201,.T.);
#784=FACE_OUTER_BOUND('',#1202,.T.);
#785=FACE_OUTER_BOUND('',#1203,.T.);
#786=FACE_OUTER_BOUND('',#1204,.T.);
#787=FACE_OUTER_BOUND('',#1205,.T.);
#788=FACE_OUTER_BOUND('',#1206,.T.);
#789=FACE_OUTER_BOUND('',#1207,.T.);
#790=FACE_OUTER_BOUND('',#1208,.T.);
#791=FACE_OUTER_BOUND('',#1209,.T.);
#792=FACE_OUTER_BOUND('',#1210,.T.);
#793=FACE_OUTER_BOUND('',#1211,.T.);
#794=FACE_OUTER_BOUND('',#1212,.T.);
#795=FACE_OUTER_BOUND('',#1213,.T.);
#796=FACE_OUTER_BOUND('',#1214,.T.);
#797=FACE_OUTER_BOUND('',#1215,.T.);
#798=FACE_OUTER_BOUND('',#1216,.T.);
#799=FACE_OUTER_BOUND('',#1217,.T.);
#800=FACE_OUTER_BOUND('',#1218,.T.);
#801=FACE_OUTER_BOUND('',#1219,.T.);
#802=FACE_OUTER_BOUND('',#1220,.T.);
#803=FACE_OUTER_BOUND('',#1221,.T.);
#804=FACE_OUTER_BOUND('',#1222,.T.);
#805=FACE_OUTER_BOUND('',#1223,.T.);
#806=FACE_OUTER_BOUND('',#1224,.T.);
#807=FACE_OUTER_BOUND('',#1225,.T.);
#808=FACE_OUTER_BOUND('',#1226,.T.);
#809=FACE_OUTER_BOUND('',#1227,.T.);
#810=FACE_OUTER_BOUND('',#1228,.T.);
#811=FACE_OUTER_BOUND('',#1229,.T.);
#812=FACE_OUTER_BOUND('',#1230,.T.);
#813=FACE_OUTER_BOUND('',#1231,.T.);
#814=FACE_OUTER_BOUND('',#1232,.T.);
#815=FACE_OUTER_BOUND('',#1233,.T.);
#1196=EDGE_LOOP('',(#5160,#5161,#5162,#5163));
#1197=EDGE_LOOP('',(#5164,#5165,#5166,#5167));
#1198=EDGE_LOOP('',(#5168,#5169,#5170,#5171));
#1199=EDGE_LOOP('',(#5172,#5173,#5174,#5175));
#1200=EDGE_LOOP('',(#5176,#5177,#5178,#5179));
#1201=EDGE_LOOP('',(#5180,#5181,#5182,#5183));
#1202=EDGE_LOOP('',(#5184,#5185,#5186,#5187));
#1203=EDGE_LOOP('',(#5188,#5189,#5190,#5191));
#1204=EDGE_LOOP('',(#5192,#5193,#5194,#5195));
#1205=EDGE_LOOP('',(#5196,#5197,#5198,#5199));
#1206=EDGE_LOOP('',(#5200,#5201,#5202,#5203));
#1207=EDGE_LOOP('',(#5204,#5205,#5206,#5207));
#1208=EDGE_LOOP('',(#5208,#5209,#5210,#5211));
#1209=EDGE_LOOP('',(#5212,#5213,#5214,#5215));
#1210=EDGE_LOOP('',(#5216,#5217,#5218,#5219));
#1211=EDGE_LOOP('',(#5220,#5221,#5222,#5223));
#1212=EDGE_LOOP('',(#5224,#5225,#5226,#5227));
#1213=EDGE_LOOP('',(#5228,#5229,#5230,#5231));
#1214=EDGE_LOOP('',(#5232,#5233,#5234,#5235,#5236,#5237,#5238,#5239,#5240,
#5241,#5242,#5243));
#1215=EDGE_LOOP('',(#5244,#5245,#5246,#5247));
#1216=EDGE_LOOP('',(#5248,#5249,#5250,#5251));
#1217=EDGE_LOOP('',(#5252,#5253,#5254,#5255));
#1218=EDGE_LOOP('',(#5256,#5257,#5258,#5259));
#1219=EDGE_LOOP('',(#5260,#5261,#5262,#5263));
#1220=EDGE_LOOP('',(#5264,#5265,#5266,#5267));
#1221=EDGE_LOOP('',(#5268,#5269,#5270,#5271));
#1222=EDGE_LOOP('',(#5272,#5273,#5274,#5275));
#1223=EDGE_LOOP('',(#5276,#5277,#5278,#5279));
#1224=EDGE_LOOP('',(#5280,#5281,#5282,#5283));
#1225=EDGE_LOOP('',(#5284,#5285,#5286,#5287));
#1226=EDGE_LOOP('',(#5288,#5289,#5290,#5291));
#1227=EDGE_LOOP('',(#5292,#5293,#5294,#5295));
#1228=EDGE_LOOP('',(#5296,#5297,#5298,#5299));
#1229=EDGE_LOOP('',(#5300,#5301,#5302,#5303));
#1230=EDGE_LOOP('',(#5304,#5305,#5306,#5307,#5308,#5309,#5310,#5311,#5312,
#5313,#5314,#5315));
#1231=EDGE_LOOP('',(#5316,#5317,#5318,#5319));
#1232=EDGE_LOOP('',(#5320,#5321,#5322,#5323));
#1233=EDGE_LOOP('',(#5324,#5325,#5326,#5327));
#1724=LINE('',#9931,#2274);
#1725=LINE('',#9935,#2275);
#1726=LINE('',#9940,#2276);
#1727=LINE('',#9944,#2277);
#1728=LINE('',#9948,#2278);
#1729=LINE('',#9951,#2279);
#1730=LINE('',#9954,#2280);
#1731=LINE('',#9957,#2281);
#1732=LINE('',#9960,#2282);
#1733=LINE('',#9963,#2283);
#1734=LINE('',#9966,#2284);
#1735=LINE('',#9969,#2285);
#1736=LINE('',#9972,#2286);
#1737=LINE('',#9974,#2287);
#1738=LINE('',#9978,#2288);
#1739=LINE('',#9980,#2289);
#1740=LINE('',#9984,#2290);
#1741=LINE('',#9986,#2291);
#1742=LINE('',#9990,#2292);
#1743=LINE('',#9992,#2293);
#1744=LINE('',#9995,#2294);
#1745=LINE('',#9996,#2295);
#1746=LINE('',#9998,#2296);
#1747=LINE('',#9999,#2297);
#1748=LINE('',#10002,#2298);
#1749=LINE('',#10004,#2299);
#1750=LINE('',#10005,#2300);
#1751=LINE('',#10008,#2301);
#1752=LINE('',#10009,#2302);
#1753=LINE('',#10012,#2303);
#1754=LINE('',#10013,#2304);
#1755=LINE('',#10016,#2305);
#1756=LINE('',#10017,#2306);
#1757=LINE('',#10020,#2307);
#1758=LINE('',#10021,#2308);
#1759=LINE('',#10024,#2309);
#1760=LINE('',#10025,#2310);
#1761=LINE('',#10030,#2311);
#1762=LINE('',#10035,#2312);
#1763=LINE('',#10039,#2313);
#1764=LINE('',#10043,#2314);
#1765=LINE('',#10047,#2315);
#1766=LINE('',#10050,#2316);
#1767=LINE('',#10053,#2317);
#1768=LINE('',#10055,#2318);
#1769=LINE('',#10059,#2319);
#1770=LINE('',#10061,#2320);
#1771=LINE('',#10065,#2321);
#1772=LINE('',#10067,#2322);
#1773=LINE('',#10071,#2323);
#1774=LINE('',#10073,#2324);
#1775=LINE('',#10076,#2325);
#1776=LINE('',#10078,#2326);
#1777=LINE('',#10082,#2327);
#1778=LINE('',#10085,#2328);
#1779=LINE('',#10087,#2329);
#1780=LINE('',#10088,#2330);
#1781=LINE('',#10090,#2331);
#1782=LINE('',#10094,#2332);
#1783=LINE('',#10095,#2333);
#2274=VECTOR('',#8214,10.);
#2275=VECTOR('',#8217,10.);
#2276=VECTOR('',#8222,10.);
#2277=VECTOR('',#8225,10.);
#2278=VECTOR('',#8230,10.);
#2279=VECTOR('',#8233,10.);
#2280=VECTOR('',#8236,10.);
#2281=VECTOR('',#8239,10.);
#2282=VECTOR('',#8242,10.);
#2283=VECTOR('',#8245,10.);
#2284=VECTOR('',#8248,10.);
#2285=VECTOR('',#8251,10.);
#2286=VECTOR('',#8254,10.);
#2287=VECTOR('',#8255,10.);
#2288=VECTOR('',#8260,10.);
#2289=VECTOR('',#8261,10.);
#2290=VECTOR('',#8266,10.);
#2291=VECTOR('',#8267,10.);
#2292=VECTOR('',#8272,10.);
#2293=VECTOR('',#8273,10.);
#2294=VECTOR('',#8278,10.);
#2295=VECTOR('',#8279,10.);
#2296=VECTOR('',#8282,10.);
#2297=VECTOR('',#8283,10.);
#2298=VECTOR('',#8286,10.);
#2299=VECTOR('',#8287,10.);
#2300=VECTOR('',#8288,10.);
#2301=VECTOR('',#8291,10.);
#2302=VECTOR('',#8292,10.);
#2303=VECTOR('',#8295,10.);
#2304=VECTOR('',#8296,10.);
#2305=VECTOR('',#8299,10.);
#2306=VECTOR('',#8300,10.);
#2307=VECTOR('',#8303,10.);
#2308=VECTOR('',#8304,10.);
#2309=VECTOR('',#8307,10.);
#2310=VECTOR('',#8308,10.);
#2311=VECTOR('',#8313,10.);
#2312=VECTOR('',#8320,10.);
#2313=VECTOR('',#8325,10.);
#2314=VECTOR('',#8330,10.);
#2315=VECTOR('',#8335,10.);
#2316=VECTOR('',#8338,10.);
#2317=VECTOR('',#8341,10.);
#2318=VECTOR('',#8342,10.);
#2319=VECTOR('',#8347,10.);
#2320=VECTOR('',#8348,10.);
#2321=VECTOR('',#8353,10.);
#2322=VECTOR('',#8354,10.);
#2323=VECTOR('',#8359,10.);
#2324=VECTOR('',#8360,10.);
#2325=VECTOR('',#8365,10.);
#2326=VECTOR('',#8366,10.);
#2327=VECTOR('',#8371,10.);
#2328=VECTOR('',#8376,10.);
#2329=VECTOR('',#8379,10.);
#2330=VECTOR('',#8380,10.);
#2331=VECTOR('',#8383,10.);
#2332=VECTOR('',#8390,10.);
#2333=VECTOR('',#8391,10.);
#2862=VERTEX_POINT('',#9929);
#2863=VERTEX_POINT('',#9930);
#2864=VERTEX_POINT('',#9932);
#2865=VERTEX_POINT('',#9934);
#2866=VERTEX_POINT('',#9938);
#2867=VERTEX_POINT('',#9939);
#2868=VERTEX_POINT('',#9941);
#2869=VERTEX_POINT('',#9943);
#2870=VERTEX_POINT('',#9947);
#2871=VERTEX_POINT('',#9949);
#2872=VERTEX_POINT('',#9953);
#2873=VERTEX_POINT('',#9955);
#2874=VERTEX_POINT('',#9959);
#2875=VERTEX_POINT('',#9961);
#2876=VERTEX_POINT('',#9965);
#2877=VERTEX_POINT('',#9967);
#2878=VERTEX_POINT('',#9971);
#2879=VERTEX_POINT('',#9973);
#2880=VERTEX_POINT('',#9977);
#2881=VERTEX_POINT('',#9979);
#2882=VERTEX_POINT('',#9983);
#2883=VERTEX_POINT('',#9985);
#2884=VERTEX_POINT('',#9989);
#2885=VERTEX_POINT('',#9991);
#2886=VERTEX_POINT('',#10001);
#2887=VERTEX_POINT('',#10003);
#2888=VERTEX_POINT('',#10007);
#2889=VERTEX_POINT('',#10011);
#2890=VERTEX_POINT('',#10015);
#2891=VERTEX_POINT('',#10019);
#2892=VERTEX_POINT('',#10023);
#2893=VERTEX_POINT('',#10028);
#2894=VERTEX_POINT('',#10029);
#2895=VERTEX_POINT('',#10034);
#2896=VERTEX_POINT('',#10038);
#2897=VERTEX_POINT('',#10042);
#2898=VERTEX_POINT('',#10046);
#2899=VERTEX_POINT('',#10048);
#2900=VERTEX_POINT('',#10052);
#2901=VERTEX_POINT('',#10054);
#2902=VERTEX_POINT('',#10058);
#2903=VERTEX_POINT('',#10060);
#2904=VERTEX_POINT('',#10064);
#2905=VERTEX_POINT('',#10066);
#2906=VERTEX_POINT('',#10070);
#2907=VERTEX_POINT('',#10072);
#2908=VERTEX_POINT('',#10077);
#2909=VERTEX_POINT('',#10081);
#3632=EDGE_CURVE('',#2862,#2863,#1724,.T.);
#3633=EDGE_CURVE('',#2863,#2864,#183,.T.);
#3634=EDGE_CURVE('',#2864,#2865,#1725,.T.);
#3635=EDGE_CURVE('',#2865,#2862,#184,.T.);
#3636=EDGE_CURVE('',#2866,#2867,#1726,.T.);
#3637=EDGE_CURVE('',#2867,#2868,#185,.T.);
#3638=EDGE_CURVE('',#2868,#2869,#1727,.T.);
#3639=EDGE_CURVE('',#2869,#2866,#186,.T.);
#3640=EDGE_CURVE('',#2867,#2870,#1728,.T.);
#3641=EDGE_CURVE('',#2870,#2871,#187,.T.);
#3642=EDGE_CURVE('',#2871,#2868,#1729,.T.);
#3643=EDGE_CURVE('',#2870,#2872,#1730,.T.);
#3644=EDGE_CURVE('',#2872,#2873,#188,.T.);
#3645=EDGE_CURVE('',#2873,#2871,#1731,.T.);
#3646=EDGE_CURVE('',#2872,#2874,#1732,.T.);
#3647=EDGE_CURVE('',#2874,#2875,#189,.T.);
#3648=EDGE_CURVE('',#2875,#2873,#1733,.T.);
#3649=EDGE_CURVE('',#2874,#2876,#1734,.T.);
#3650=EDGE_CURVE('',#2876,#2877,#190,.T.);
#3651=EDGE_CURVE('',#2877,#2875,#1735,.T.);
#3652=EDGE_CURVE('',#2878,#2877,#1736,.T.);
#3653=EDGE_CURVE('',#2876,#2879,#1737,.T.);
#3654=EDGE_CURVE('',#2879,#2878,#191,.T.);
#3655=EDGE_CURVE('',#2880,#2878,#1738,.T.);
#3656=EDGE_CURVE('',#2879,#2881,#1739,.T.);
#3657=EDGE_CURVE('',#2881,#2880,#192,.T.);
#3658=EDGE_CURVE('',#2882,#2880,#1740,.T.);
#3659=EDGE_CURVE('',#2881,#2883,#1741,.T.);
#3660=EDGE_CURVE('',#2883,#2882,#193,.T.);
#3661=EDGE_CURVE('',#2884,#2882,#1742,.T.);
#3662=EDGE_CURVE('',#2883,#2885,#1743,.T.);
#3663=EDGE_CURVE('',#2885,#2884,#194,.T.);
#3664=EDGE_CURVE('',#2863,#2884,#1744,.T.);
#3665=EDGE_CURVE('',#2885,#2864,#1745,.T.);
#3666=EDGE_CURVE('',#2869,#2862,#1746,.T.);
#3667=EDGE_CURVE('',#2865,#2866,#1747,.T.);
#3668=EDGE_CURVE('',#2882,#2886,#1748,.T.);
#3669=EDGE_CURVE('',#2887,#2886,#1749,.T.);
#3670=EDGE_CURVE('',#2887,#2880,#1750,.T.);
#3671=EDGE_CURVE('',#2888,#2884,#1751,.T.);
#3672=EDGE_CURVE('',#2886,#2888,#1752,.T.);
#3673=EDGE_CURVE('',#2863,#2889,#1753,.T.);
#3674=EDGE_CURVE('',#2888,#2889,#1754,.T.);
#3675=EDGE_CURVE('',#2890,#2862,#1755,.T.);
#3676=EDGE_CURVE('',#2889,#2890,#1756,.T.);
#3677=EDGE_CURVE('',#2869,#2891,#1757,.T.);
#3678=EDGE_CURVE('',#2890,#2891,#1758,.T.);
#3679=EDGE_CURVE('',#2892,#2868,#1759,.T.);
#3680=EDGE_CURVE('',#2891,#2892,#1760,.T.);
#3681=EDGE_CURVE('',#2893,#2894,#1761,.T.);
#3682=EDGE_CURVE('',#2894,#2889,#195,.T.);
#3683=EDGE_CURVE('',#2893,#2890,#196,.T.);
#3684=EDGE_CURVE('',#2894,#2895,#1762,.T.);
#3685=EDGE_CURVE('',#2895,#2888,#197,.T.);
#3686=EDGE_CURVE('',#2895,#2896,#1763,.T.);
#3687=EDGE_CURVE('',#2896,#2886,#198,.T.);
#3688=EDGE_CURVE('',#2896,#2897,#1764,.T.);
#3689=EDGE_CURVE('',#2897,#2887,#199,.T.);
#3690=EDGE_CURVE('',#2897,#2898,#1765,.T.);
#3691=EDGE_CURVE('',#2898,#2899,#200,.T.);
#3692=EDGE_CURVE('',#2899,#2887,#1766,.T.);
#3693=EDGE_CURVE('',#2900,#2899,#1767,.T.);
#3694=EDGE_CURVE('',#2898,#2901,#1768,.T.);
#3695=EDGE_CURVE('',#2901,#2900,#201,.T.);
#3696=EDGE_CURVE('',#2902,#2900,#1769,.T.);
#3697=EDGE_CURVE('',#2901,#2903,#1770,.T.);
#3698=EDGE_CURVE('',#2903,#2902,#202,.T.);
#3699=EDGE_CURVE('',#2904,#2902,#1771,.T.);
#3700=EDGE_CURVE('',#2903,#2905,#1772,.T.);
#3701=EDGE_CURVE('',#2905,#2904,#203,.T.);
#3702=EDGE_CURVE('',#2906,#2904,#1773,.T.);
#3703=EDGE_CURVE('',#2905,#2907,#1774,.T.);
#3704=EDGE_CURVE('',#2907,#2906,#204,.T.);
#3705=EDGE_CURVE('',#2892,#2906,#1775,.T.);
#3706=EDGE_CURVE('',#2907,#2908,#1776,.T.);
#3707=EDGE_CURVE('',#2908,#2892,#205,.T.);
#3708=EDGE_CURVE('',#2908,#2909,#1777,.T.);
#3709=EDGE_CURVE('',#2909,#2891,#206,.T.);
#3710=EDGE_CURVE('',#2909,#2893,#1778,.T.);
#3711=EDGE_CURVE('',#2875,#2902,#1779,.T.);
#3712=EDGE_CURVE('',#2904,#2873,#1780,.T.);
#3713=EDGE_CURVE('',#2871,#2906,#1781,.T.);
#3714=EDGE_CURVE('',#2878,#2899,#1782,.T.);
#3715=EDGE_CURVE('',#2900,#2877,#1783,.T.);
#5160=ORIENTED_EDGE('',*,*,#3632,.T.);
#5161=ORIENTED_EDGE('',*,*,#3633,.T.);
#5162=ORIENTED_EDGE('',*,*,#3634,.T.);
#5163=ORIENTED_EDGE('',*,*,#3635,.T.);
#5164=ORIENTED_EDGE('',*,*,#3636,.T.);
#5165=ORIENTED_EDGE('',*,*,#3637,.T.);
#5166=ORIENTED_EDGE('',*,*,#3638,.T.);
#5167=ORIENTED_EDGE('',*,*,#3639,.T.);
#5168=ORIENTED_EDGE('',*,*,#3640,.T.);
#5169=ORIENTED_EDGE('',*,*,#3641,.T.);
#5170=ORIENTED_EDGE('',*,*,#3642,.T.);
#5171=ORIENTED_EDGE('',*,*,#3637,.F.);
#5172=ORIENTED_EDGE('',*,*,#3643,.T.);
#5173=ORIENTED_EDGE('',*,*,#3644,.T.);
#5174=ORIENTED_EDGE('',*,*,#3645,.T.);
#5175=ORIENTED_EDGE('',*,*,#3641,.F.);
#5176=ORIENTED_EDGE('',*,*,#3646,.T.);
#5177=ORIENTED_EDGE('',*,*,#3647,.T.);
#5178=ORIENTED_EDGE('',*,*,#3648,.T.);
#5179=ORIENTED_EDGE('',*,*,#3644,.F.);
#5180=ORIENTED_EDGE('',*,*,#3649,.T.);
#5181=ORIENTED_EDGE('',*,*,#3650,.T.);
#5182=ORIENTED_EDGE('',*,*,#3651,.T.);
#5183=ORIENTED_EDGE('',*,*,#3647,.F.);
#5184=ORIENTED_EDGE('',*,*,#3652,.T.);
#5185=ORIENTED_EDGE('',*,*,#3650,.F.);
#5186=ORIENTED_EDGE('',*,*,#3653,.T.);
#5187=ORIENTED_EDGE('',*,*,#3654,.T.);
#5188=ORIENTED_EDGE('',*,*,#3655,.T.);
#5189=ORIENTED_EDGE('',*,*,#3654,.F.);
#5190=ORIENTED_EDGE('',*,*,#3656,.T.);
#5191=ORIENTED_EDGE('',*,*,#3657,.T.);
#5192=ORIENTED_EDGE('',*,*,#3658,.T.);
#5193=ORIENTED_EDGE('',*,*,#3657,.F.);
#5194=ORIENTED_EDGE('',*,*,#3659,.T.);
#5195=ORIENTED_EDGE('',*,*,#3660,.T.);
#5196=ORIENTED_EDGE('',*,*,#3661,.T.);
#5197=ORIENTED_EDGE('',*,*,#3660,.F.);
#5198=ORIENTED_EDGE('',*,*,#3662,.T.);
#5199=ORIENTED_EDGE('',*,*,#3663,.T.);
#5200=ORIENTED_EDGE('',*,*,#3664,.T.);
#5201=ORIENTED_EDGE('',*,*,#3663,.F.);
#5202=ORIENTED_EDGE('',*,*,#3665,.T.);
#5203=ORIENTED_EDGE('',*,*,#3633,.F.);
#5204=ORIENTED_EDGE('',*,*,#3666,.T.);
#5205=ORIENTED_EDGE('',*,*,#3635,.F.);
#5206=ORIENTED_EDGE('',*,*,#3667,.T.);
#5207=ORIENTED_EDGE('',*,*,#3639,.F.);
#5208=ORIENTED_EDGE('',*,*,#3658,.F.);
#5209=ORIENTED_EDGE('',*,*,#3668,.T.);
#5210=ORIENTED_EDGE('',*,*,#3669,.F.);
#5211=ORIENTED_EDGE('',*,*,#3670,.T.);
#5212=ORIENTED_EDGE('',*,*,#3661,.F.);
#5213=ORIENTED_EDGE('',*,*,#3671,.F.);
#5214=ORIENTED_EDGE('',*,*,#3672,.F.);
#5215=ORIENTED_EDGE('',*,*,#3668,.F.);
#5216=ORIENTED_EDGE('',*,*,#3664,.F.);
#5217=ORIENTED_EDGE('',*,*,#3673,.T.);
#5218=ORIENTED_EDGE('',*,*,#3674,.F.);
#5219=ORIENTED_EDGE('',*,*,#3671,.T.);
#5220=ORIENTED_EDGE('',*,*,#3632,.F.);
#5221=ORIENTED_EDGE('',*,*,#3675,.F.);
#5222=ORIENTED_EDGE('',*,*,#3676,.F.);
#5223=ORIENTED_EDGE('',*,*,#3673,.F.);
#5224=ORIENTED_EDGE('',*,*,#3666,.F.);
#5225=ORIENTED_EDGE('',*,*,#3677,.T.);
#5226=ORIENTED_EDGE('',*,*,#3678,.F.);
#5227=ORIENTED_EDGE('',*,*,#3675,.T.);
#5228=ORIENTED_EDGE('',*,*,#3638,.F.);
#5229=ORIENTED_EDGE('',*,*,#3679,.F.);
#5230=ORIENTED_EDGE('',*,*,#3680,.F.);
#5231=ORIENTED_EDGE('',*,*,#3677,.F.);
#5232=ORIENTED_EDGE('',*,*,#3636,.F.);
#5233=ORIENTED_EDGE('',*,*,#3667,.F.);
#5234=ORIENTED_EDGE('',*,*,#3634,.F.);
#5235=ORIENTED_EDGE('',*,*,#3665,.F.);
#5236=ORIENTED_EDGE('',*,*,#3662,.F.);
#5237=ORIENTED_EDGE('',*,*,#3659,.F.);
#5238=ORIENTED_EDGE('',*,*,#3656,.F.);
#5239=ORIENTED_EDGE('',*,*,#3653,.F.);
#5240=ORIENTED_EDGE('',*,*,#3649,.F.);
#5241=ORIENTED_EDGE('',*,*,#3646,.F.);
#5242=ORIENTED_EDGE('',*,*,#3643,.F.);
#5243=ORIENTED_EDGE('',*,*,#3640,.F.);
#5244=ORIENTED_EDGE('',*,*,#3681,.T.);
#5245=ORIENTED_EDGE('',*,*,#3682,.T.);
#5246=ORIENTED_EDGE('',*,*,#3676,.T.);
#5247=ORIENTED_EDGE('',*,*,#3683,.F.);
#5248=ORIENTED_EDGE('',*,*,#3684,.T.);
#5249=ORIENTED_EDGE('',*,*,#3685,.T.);
#5250=ORIENTED_EDGE('',*,*,#3674,.T.);
#5251=ORIENTED_EDGE('',*,*,#3682,.F.);
#5252=ORIENTED_EDGE('',*,*,#3686,.T.);
#5253=ORIENTED_EDGE('',*,*,#3687,.T.);
#5254=ORIENTED_EDGE('',*,*,#3672,.T.);
#5255=ORIENTED_EDGE('',*,*,#3685,.F.);
#5256=ORIENTED_EDGE('',*,*,#3688,.T.);
#5257=ORIENTED_EDGE('',*,*,#3689,.T.);
#5258=ORIENTED_EDGE('',*,*,#3669,.T.);
#5259=ORIENTED_EDGE('',*,*,#3687,.F.);
#5260=ORIENTED_EDGE('',*,*,#3690,.T.);
#5261=ORIENTED_EDGE('',*,*,#3691,.T.);
#5262=ORIENTED_EDGE('',*,*,#3692,.T.);
#5263=ORIENTED_EDGE('',*,*,#3689,.F.);
#5264=ORIENTED_EDGE('',*,*,#3693,.T.);
#5265=ORIENTED_EDGE('',*,*,#3691,.F.);
#5266=ORIENTED_EDGE('',*,*,#3694,.T.);
#5267=ORIENTED_EDGE('',*,*,#3695,.T.);
#5268=ORIENTED_EDGE('',*,*,#3696,.T.);
#5269=ORIENTED_EDGE('',*,*,#3695,.F.);
#5270=ORIENTED_EDGE('',*,*,#3697,.T.);
#5271=ORIENTED_EDGE('',*,*,#3698,.T.);
#5272=ORIENTED_EDGE('',*,*,#3699,.T.);
#5273=ORIENTED_EDGE('',*,*,#3698,.F.);
#5274=ORIENTED_EDGE('',*,*,#3700,.T.);
#5275=ORIENTED_EDGE('',*,*,#3701,.T.);
#5276=ORIENTED_EDGE('',*,*,#3702,.T.);
#5277=ORIENTED_EDGE('',*,*,#3701,.F.);
#5278=ORIENTED_EDGE('',*,*,#3703,.T.);
#5279=ORIENTED_EDGE('',*,*,#3704,.T.);
#5280=ORIENTED_EDGE('',*,*,#3705,.T.);
#5281=ORIENTED_EDGE('',*,*,#3704,.F.);
#5282=ORIENTED_EDGE('',*,*,#3706,.T.);
#5283=ORIENTED_EDGE('',*,*,#3707,.T.);
#5284=ORIENTED_EDGE('',*,*,#3680,.T.);
#5285=ORIENTED_EDGE('',*,*,#3707,.F.);
#5286=ORIENTED_EDGE('',*,*,#3708,.T.);
#5287=ORIENTED_EDGE('',*,*,#3709,.T.);
#5288=ORIENTED_EDGE('',*,*,#3678,.T.);
#5289=ORIENTED_EDGE('',*,*,#3709,.F.);
#5290=ORIENTED_EDGE('',*,*,#3710,.T.);
#5291=ORIENTED_EDGE('',*,*,#3683,.T.);
#5292=ORIENTED_EDGE('',*,*,#3648,.F.);
#5293=ORIENTED_EDGE('',*,*,#3711,.T.);
#5294=ORIENTED_EDGE('',*,*,#3699,.F.);
#5295=ORIENTED_EDGE('',*,*,#3712,.T.);
#5296=ORIENTED_EDGE('',*,*,#3645,.F.);
#5297=ORIENTED_EDGE('',*,*,#3712,.F.);
#5298=ORIENTED_EDGE('',*,*,#3702,.F.);
#5299=ORIENTED_EDGE('',*,*,#3713,.F.);
#5300=ORIENTED_EDGE('',*,*,#3642,.F.);
#5301=ORIENTED_EDGE('',*,*,#3713,.T.);
#5302=ORIENTED_EDGE('',*,*,#3705,.F.);
#5303=ORIENTED_EDGE('',*,*,#3679,.T.);
#5304=ORIENTED_EDGE('',*,*,#3681,.F.);
#5305=ORIENTED_EDGE('',*,*,#3710,.F.);
#5306=ORIENTED_EDGE('',*,*,#3708,.F.);
#5307=ORIENTED_EDGE('',*,*,#3706,.F.);
#5308=ORIENTED_EDGE('',*,*,#3703,.F.);
#5309=ORIENTED_EDGE('',*,*,#3700,.F.);
#5310=ORIENTED_EDGE('',*,*,#3697,.F.);
#5311=ORIENTED_EDGE('',*,*,#3694,.F.);
#5312=ORIENTED_EDGE('',*,*,#3690,.F.);
#5313=ORIENTED_EDGE('',*,*,#3688,.F.);
#5314=ORIENTED_EDGE('',*,*,#3686,.F.);
#5315=ORIENTED_EDGE('',*,*,#3684,.F.);
#5316=ORIENTED_EDGE('',*,*,#3652,.F.);
#5317=ORIENTED_EDGE('',*,*,#3714,.T.);
#5318=ORIENTED_EDGE('',*,*,#3693,.F.);
#5319=ORIENTED_EDGE('',*,*,#3715,.T.);
#5320=ORIENTED_EDGE('',*,*,#3651,.F.);
#5321=ORIENTED_EDGE('',*,*,#3715,.F.);
#5322=ORIENTED_EDGE('',*,*,#3696,.F.);
#5323=ORIENTED_EDGE('',*,*,#3711,.F.);
#5324=ORIENTED_EDGE('',*,*,#3655,.F.);
#5325=ORIENTED_EDGE('',*,*,#3670,.F.);
#5326=ORIENTED_EDGE('',*,*,#3692,.F.);
#5327=ORIENTED_EDGE('',*,*,#3714,.F.);
#5506=CYLINDRICAL_SURFACE('',#6550,1.);
#5507=CYLINDRICAL_SURFACE('',#6553,1.);
#5508=CYLINDRICAL_SURFACE('',#6556,1.);
#5509=CYLINDRICAL_SURFACE('',#6558,1.);
#5510=CYLINDRICAL_SURFACE('',#6560,1.);
#5511=CYLINDRICAL_SURFACE('',#6562,1.);
#5512=CYLINDRICAL_SURFACE('',#6564,1.);
#5513=CYLINDRICAL_SURFACE('',#6566,1.);
#5514=CYLINDRICAL_SURFACE('',#6568,1.);
#5515=CYLINDRICAL_SURFACE('',#6570,1.);
#5516=CYLINDRICAL_SURFACE('',#6572,1.);
#5517=CYLINDRICAL_SURFACE('',#6573,1.);
#5518=CYLINDRICAL_SURFACE('',#6581,1.);
#5519=CYLINDRICAL_SURFACE('',#6584,1.);
#5520=CYLINDRICAL_SURFACE('',#6586,1.);
#5521=CYLINDRICAL_SURFACE('',#6588,1.);
#5522=CYLINDRICAL_SURFACE('',#6590,1.);
#5523=CYLINDRICAL_SURFACE('',#6592,1.);
#5524=CYLINDRICAL_SURFACE('',#6594,1.);
#5525=CYLINDRICAL_SURFACE('',#6596,1.);
#5526=CYLINDRICAL_SURFACE('',#6598,1.);
#5527=CYLINDRICAL_SURFACE('',#6600,1.);
#5528=CYLINDRICAL_SURFACE('',#6602,1.);
#5529=CYLINDRICAL_SURFACE('',#6604,1.);
#5841=ADVANCED_FACE('',(#778),#5506,.T.);
#5842=ADVANCED_FACE('',(#779),#5507,.T.);
#5843=ADVANCED_FACE('',(#780),#5508,.T.);
#5844=ADVANCED_FACE('',(#781),#5509,.T.);
#5845=ADVANCED_FACE('',(#782),#5510,.T.);
#5846=ADVANCED_FACE('',(#783),#5511,.T.);
#5847=ADVANCED_FACE('',(#784),#5512,.T.);
#5848=ADVANCED_FACE('',(#785),#5513,.T.);
#5849=ADVANCED_FACE('',(#786),#5514,.T.);
#5850=ADVANCED_FACE('',(#787),#5515,.T.);
#5851=ADVANCED_FACE('',(#788),#5516,.T.);
#5852=ADVANCED_FACE('',(#789),#5517,.T.);
#5853=ADVANCED_FACE('',(#790),#453,.T.);
#5854=ADVANCED_FACE('',(#791),#454,.T.);
#5855=ADVANCED_FACE('',(#792),#455,.T.);
#5856=ADVANCED_FACE('',(#793),#456,.T.);
#5857=ADVANCED_FACE('',(#794),#457,.T.);
#5858=ADVANCED_FACE('',(#795),#458,.T.);
#5859=ADVANCED_FACE('',(#796),#459,.F.);
#5860=ADVANCED_FACE('',(#797),#5518,.T.);
#5861=ADVANCED_FACE('',(#798),#5519,.T.);
#5862=ADVANCED_FACE('',(#799),#5520,.T.);
#5863=ADVANCED_FACE('',(#800),#5521,.T.);
#5864=ADVANCED_FACE('',(#801),#5522,.T.);
#5865=ADVANCED_FACE('',(#802),#5523,.T.);
#5866=ADVANCED_FACE('',(#803),#5524,.T.);
#5867=ADVANCED_FACE('',(#804),#5525,.T.);
#5868=ADVANCED_FACE('',(#805),#5526,.T.);
#5869=ADVANCED_FACE('',(#806),#5527,.T.);
#5870=ADVANCED_FACE('',(#807),#5528,.T.);
#5871=ADVANCED_FACE('',(#808),#5529,.T.);
#5872=ADVANCED_FACE('',(#809),#460,.T.);
#5873=ADVANCED_FACE('',(#810),#461,.T.);
#5874=ADVANCED_FACE('',(#811),#462,.T.);
#5875=ADVANCED_FACE('',(#812),#463,.T.);
#5876=ADVANCED_FACE('',(#813),#464,.T.);
#5877=ADVANCED_FACE('',(#814),#465,.T.);
#5878=ADVANCED_FACE('',(#815),#466,.T.);
#5888=CLOSED_SHELL('',(#5841,#5842,#5843,#5844,#5845,#5846,#5847,#5848,
#5849,#5850,#5851,#5852,#5853,#5854,#5855,#5856,#5857,#5858,#5859,#5860,
#5861,#5862,#5863,#5864,#5865,#5866,#5867,#5868,#5869,#5870,#5871,#5872,
#5873,#5874,#5875,#5876,#5877,#5878));
#6549=AXIS2_PLACEMENT_3D('',#9927,#8210,#8211);
#6550=AXIS2_PLACEMENT_3D('',#9928,#8212,#8213);
#6551=AXIS2_PLACEMENT_3D('',#9933,#8215,#8216);
#6552=AXIS2_PLACEMENT_3D('',#9936,#8218,#8219);
#6553=AXIS2_PLACEMENT_3D('',#9937,#8220,#8221);
#6554=AXIS2_PLACEMENT_3D('',#9942,#8223,#8224);
#6555=AXIS2_PLACEMENT_3D('',#9945,#8226,#8227);
#6556=AXIS2_PLACEMENT_3D('',#9946,#8228,#8229);
#6557=AXIS2_PLACEMENT_3D('',#9950,#8231,#8232);
#6558=AXIS2_PLACEMENT_3D('',#9952,#8234,#8235);
#6559=AXIS2_PLACEMENT_3D('',#9956,#8237,#8238);
#6560=AXIS2_PLACEMENT_3D('',#9958,#8240,#8241);
#6561=AXIS2_PLACEMENT_3D('',#9962,#8243,#8244);
#6562=AXIS2_PLACEMENT_3D('',#9964,#8246,#8247);
#6563=AXIS2_PLACEMENT_3D('',#9968,#8249,#8250);
#6564=AXIS2_PLACEMENT_3D('',#9970,#8252,#8253);
#6565=AXIS2_PLACEMENT_3D('',#9975,#8256,#8257);
#6566=AXIS2_PLACEMENT_3D('',#9976,#8258,#8259);
#6567=AXIS2_PLACEMENT_3D('',#9981,#8262,#8263);
#6568=AXIS2_PLACEMENT_3D('',#9982,#8264,#8265);
#6569=AXIS2_PLACEMENT_3D('',#9987,#8268,#8269);
#6570=AXIS2_PLACEMENT_3D('',#9988,#8270,#8271);
#6571=AXIS2_PLACEMENT_3D('',#9993,#8274,#8275);
#6572=AXIS2_PLACEMENT_3D('',#9994,#8276,#8277);
#6573=AXIS2_PLACEMENT_3D('',#9997,#8280,#8281);
#6574=AXIS2_PLACEMENT_3D('',#10000,#8284,#8285);
#6575=AXIS2_PLACEMENT_3D('',#10006,#8289,#8290);
#6576=AXIS2_PLACEMENT_3D('',#10010,#8293,#8294);
#6577=AXIS2_PLACEMENT_3D('',#10014,#8297,#8298);
#6578=AXIS2_PLACEMENT_3D('',#10018,#8301,#8302);
#6579=AXIS2_PLACEMENT_3D('',#10022,#8305,#8306);
#6580=AXIS2_PLACEMENT_3D('',#10026,#8309,#8310);
#6581=AXIS2_PLACEMENT_3D('',#10027,#8311,#8312);
#6582=AXIS2_PLACEMENT_3D('',#10031,#8314,#8315);
#6583=AXIS2_PLACEMENT_3D('',#10032,#8316,#8317);
#6584=AXIS2_PLACEMENT_3D('',#10033,#8318,#8319);
#6585=AXIS2_PLACEMENT_3D('',#10036,#8321,#8322);
#6586=AXIS2_PLACEMENT_3D('',#10037,#8323,#8324);
#6587=AXIS2_PLACEMENT_3D('',#10040,#8326,#8327);
#6588=AXIS2_PLACEMENT_3D('',#10041,#8328,#8329);
#6589=AXIS2_PLACEMENT_3D('',#10044,#8331,#8332);
#6590=AXIS2_PLACEMENT_3D('',#10045,#8333,#8334);
#6591=AXIS2_PLACEMENT_3D('',#10049,#8336,#8337);
#6592=AXIS2_PLACEMENT_3D('',#10051,#8339,#8340);
#6593=AXIS2_PLACEMENT_3D('',#10056,#8343,#8344);
#6594=AXIS2_PLACEMENT_3D('',#10057,#8345,#8346);
#6595=AXIS2_PLACEMENT_3D('',#10062,#8349,#8350);
#6596=AXIS2_PLACEMENT_3D('',#10063,#8351,#8352);
#6597=AXIS2_PLACEMENT_3D('',#10068,#8355,#8356);
#6598=AXIS2_PLACEMENT_3D('',#10069,#8357,#8358);
#6599=AXIS2_PLACEMENT_3D('',#10074,#8361,#8362);
#6600=AXIS2_PLACEMENT_3D('',#10075,#8363,#8364);
#6601=AXIS2_PLACEMENT_3D('',#10079,#8367,#8368);
#6602=AXIS2_PLACEMENT_3D('',#10080,#8369,#8370);
#6603=AXIS2_PLACEMENT_3D('',#10083,#8372,#8373);
#6604=AXIS2_PLACEMENT_3D('',#10084,#8374,#8375);
#6605=AXIS2_PLACEMENT_3D('',#10086,#8377,#8378);
#6606=AXIS2_PLACEMENT_3D('',#10089,#8381,#8382);
#6607=AXIS2_PLACEMENT_3D('',#10091,#8384,#8385);
#6608=AXIS2_PLACEMENT_3D('',#10092,#8386,#8387);
#6609=AXIS2_PLACEMENT_3D('',#10093,#8388,#8389);
#6610=AXIS2_PLACEMENT_3D('',#10096,#8392,#8393);
#6611=AXIS2_PLACEMENT_3D('',#10097,#8394,#8395);
#8210=DIRECTION('axis',(0.,0.,1.));
#8211=DIRECTION('refdir',(1.,0.,0.));
#8212=DIRECTION('center_axis',(0.,1.,0.));
#8213=DIRECTION('ref_axis',(0.707106781186548,0.,-0.707106781186548));
#8214=DIRECTION('',(0.,-1.,0.));
#8215=DIRECTION('center_axis',(0.38268343236509,0.923879532511287,0.));
#8216=DIRECTION('ref_axis',(0.923879532511287,-0.38268343236509,0.));
#8217=DIRECTION('',(0.,1.,0.));
#8218=DIRECTION('center_axis',(-0.382683432365087,-0.923879532511288,0.));
#8219=DIRECTION('ref_axis',(0.923879532511288,-0.382683432365087,0.));
#8220=DIRECTION('center_axis',(1.,0.,0.));
#8221=DIRECTION('ref_axis',(0.,-0.707106781186548,-0.707106781186548));
#8222=DIRECTION('',(1.,0.,0.));
#8223=DIRECTION('center_axis',(-0.923879532511287,-0.38268343236509,0.));
#8224=DIRECTION('ref_axis',(-0.38268343236509,0.923879532511287,0.));
#8225=DIRECTION('',(-1.,0.,0.));
#8226=DIRECTION('center_axis',(0.923879532511288,0.382683432365087,-5.80230514691304E-15));
#8227=DIRECTION('ref_axis',(-0.382683432365087,0.923879532511288,-1.40080037787048E-14));
#8228=DIRECTION('center_axis',(0.707106781186548,0.707106781186548,0.));
#8229=DIRECTION('ref_axis',(0.499999999999998,-0.499999999999998,-0.70710678118655));
#8230=DIRECTION('',(0.707106781186548,0.707106781186548,0.));
#8231=DIRECTION('center_axis',(-0.382683432365095,-0.923879532511285,0.));
#8232=DIRECTION('ref_axis',(-0.923879532511285,0.382683432365095,0.));
#8233=DIRECTION('',(-0.707106781186548,-0.707106781186548,0.));
#8234=DIRECTION('center_axis',(0.,-1.,0.));
#8235=DIRECTION('ref_axis',(0.707106781186548,0.,-0.707106781186548));
#8236=DIRECTION('',(0.,1.,0.));
#8237=DIRECTION('center_axis',(0.382683432365099,-0.923879532511283,-8.20569863179165E-15));
#8238=DIRECTION('ref_axis',(0.923879532511283,0.382683432365098,-1.98103089256172E-14));
#8239=DIRECTION('',(0.,-1.,0.));
#8240=DIRECTION('center_axis',(-0.707106781186548,0.707106781186548,0.));
#8241=DIRECTION('ref_axis',(0.499999999999998,0.499999999999998,-0.70710678118655));
#8242=DIRECTION('',(-0.707106781186548,0.707106781186548,0.));
#8243=DIRECTION('center_axis',(0.923879532511286,-0.382683432365092,0.));
#8244=DIRECTION('ref_axis',(-0.382683432365092,-0.923879532511286,0.));
#8245=DIRECTION('',(0.707106781186548,-0.707106781186548,0.));
#8246=DIRECTION('center_axis',(1.,0.,0.));
#8247=DIRECTION('ref_axis',(0.,0.707106781186548,-0.707106781186548));
#8248=DIRECTION('',(-1.,0.,0.));
#8249=DIRECTION('center_axis',(0.923879532511286,0.382683432365092,0.));
#8250=DIRECTION('ref_axis',(-0.382683432365092,0.923879532511286,0.));
#8251=DIRECTION('',(1.,0.,0.));
#8252=DIRECTION('center_axis',(-0.707106781186548,-0.707106781186548,0.));
#8253=DIRECTION('ref_axis',(-0.499999999999998,0.499999999999998,-0.70710678118655));
#8254=DIRECTION('',(0.707106781186548,0.707106781186548,0.));
#8255=DIRECTION('',(-0.707106781186548,-0.707106781186548,0.));
#8256=DIRECTION('center_axis',(0.382683432365092,0.923879532511286,0.));
#8257=DIRECTION('ref_axis',(0.923879532511286,-0.382683432365092,0.));
#8258=DIRECTION('center_axis',(0.,1.,0.));
#8259=DIRECTION('ref_axis',(-0.707106781186548,0.,-0.707106781186548));
#8260=DIRECTION('',(0.,1.,0.));
#8261=DIRECTION('',(0.,-1.,0.));
#8262=DIRECTION('center_axis',(-0.382683432365092,0.923879532511286,0.));
#8263=DIRECTION('ref_axis',(-0.923879532511286,-0.382683432365092,0.));
#8264=DIRECTION('center_axis',(0.707106781186548,-0.707106781186548,0.));
#8265=DIRECTION('ref_axis',(-0.499999999999998,-0.499999999999998,-0.70710678118655));
#8266=DIRECTION('',(-0.707106781186548,0.707106781186548,0.));
#8267=DIRECTION('',(0.707106781186548,-0.707106781186548,0.));
#8268=DIRECTION('center_axis',(-0.923879532511286,0.382683432365092,0.));
#8269=DIRECTION('ref_axis',(0.382683432365092,0.923879532511286,0.));
#8270=DIRECTION('center_axis',(-1.,0.,0.));
#8271=DIRECTION('ref_axis',(0.,-0.707106781186548,-0.707106781186548));
#8272=DIRECTION('',(-1.,0.,0.));
#8273=DIRECTION('',(1.,0.,0.));
#8274=DIRECTION('center_axis',(-0.923879532511286,-0.382683432365092,4.10284931589584E-15));
#8275=DIRECTION('ref_axis',(0.382683432365092,-0.923879532511286,9.90515446280885E-15));
#8276=DIRECTION('center_axis',(0.707106781186548,0.707106781186548,0.));
#8277=DIRECTION('ref_axis',(0.499999999999998,-0.499999999999998,-0.70710678118655));
#8278=DIRECTION('',(-0.707106781186548,-0.707106781186548,0.));
#8279=DIRECTION('',(0.707106781186548,0.707106781186548,0.));
#8280=DIRECTION('center_axis',(0.707106781186548,0.707106781186548,0.));
#8281=DIRECTION('ref_axis',(0.499999999999998,-0.499999999999998,-0.70710678118655));
#8282=DIRECTION('',(-0.707106781186548,-0.707106781186548,0.));
#8283=DIRECTION('',(0.707106781186548,0.707106781186548,0.));
#8284=DIRECTION('center_axis',(-0.707106781186548,-0.707106781186548,0.));
#8285=DIRECTION('ref_axis',(0.,0.,1.));
#8286=DIRECTION('',(0.,0.,1.));
#8287=DIRECTION('',(0.707106781186548,-0.707106781186548,0.));
#8288=DIRECTION('',(0.,0.,-1.));
#8289=DIRECTION('center_axis',(0.,-1.,0.));
#8290=DIRECTION('ref_axis',(1.,0.,0.));
#8291=DIRECTION('',(0.,0.,-1.));
#8292=DIRECTION('',(1.,0.,0.));
#8293=DIRECTION('center_axis',(0.707106781186548,-0.707106781186548,0.));
#8294=DIRECTION('ref_axis',(0.,0.,-1.));
#8295=DIRECTION('',(0.,0.,1.));
#8296=DIRECTION('',(0.707106781186548,0.707106781186548,0.));
#8297=DIRECTION('center_axis',(1.,0.,0.));
#8298=DIRECTION('ref_axis',(0.,1.,0.));
#8299=DIRECTION('',(0.,0.,-1.));
#8300=DIRECTION('',(0.,1.,0.));
#8301=DIRECTION('center_axis',(0.707106781186548,-0.707106781186548,0.));
#8302=DIRECTION('ref_axis',(0.,0.,-1.));
#8303=DIRECTION('',(0.,0.,1.));
#8304=DIRECTION('',(0.707106781186548,0.707106781186548,0.));
#8305=DIRECTION('center_axis',(0.,-1.,0.));
#8306=DIRECTION('ref_axis',(1.,0.,0.));
#8307=DIRECTION('',(0.,0.,-1.));
#8308=DIRECTION('',(1.,0.,0.));
#8309=DIRECTION('center_axis',(0.,0.,1.));
#8310=DIRECTION('ref_axis',(-1.,0.,0.));
#8311=DIRECTION('center_axis',(0.,1.,0.));
#8312=DIRECTION('ref_axis',(0.707106781186551,0.,0.707106781186544));
#8313=DIRECTION('',(0.,-1.,0.));
#8314=DIRECTION('center_axis',(0.38268343236509,0.923879532511287,0.));
#8315=DIRECTION('ref_axis',(0.923879532511287,-0.38268343236509,0.));
#8316=DIRECTION('center_axis',(0.382683432365087,0.923879532511288,0.));
#8317=DIRECTION('ref_axis',(0.923879532511288,-0.382683432365087,0.));
#8318=DIRECTION('center_axis',(-0.707106781186548,-0.707106781186548,0.));
#8319=DIRECTION('ref_axis',(0.499999999999998,-0.499999999999998,0.70710678118655));
#8320=DIRECTION('',(-0.707106781186548,-0.707106781186548,0.));
#8321=DIRECTION('center_axis',(0.923879532511285,0.382683432365095,-4.10284931589581E-15));
#8322=DIRECTION('ref_axis',(-0.382683432365095,0.923879532511285,9.905154462809E-15));
#8323=DIRECTION('center_axis',(1.,0.,0.));
#8324=DIRECTION('ref_axis',(0.,-0.707106781186548,0.707106781186548));
#8325=DIRECTION('',(-1.,0.,0.));
#8326=DIRECTION('center_axis',(0.923879532511286,-0.382683432365092,0.));
#8327=DIRECTION('ref_axis',(-0.382683432365092,-0.923879532511286,0.));
#8328=DIRECTION('center_axis',(-0.707106781186548,0.707106781186548,0.));
#8329=DIRECTION('ref_axis',(-0.499999999999998,-0.499999999999998,0.70710678118655));
#8330=DIRECTION('',(-0.707106781186548,0.707106781186548,0.));
#8331=DIRECTION('center_axis',(0.382683432365092,-0.923879532511286,0.));
#8332=DIRECTION('ref_axis',(0.923879532511286,0.382683432365092,0.));
#8333=DIRECTION('center_axis',(0.,-1.,0.));
#8334=DIRECTION('ref_axis',(-0.707106781186548,0.,0.707106781186548));
#8335=DIRECTION('',(0.,1.,0.));
#8336=DIRECTION('center_axis',(-0.382683432365092,-0.923879532511286,0.));
#8337=DIRECTION('ref_axis',(-0.923879532511286,0.382683432365092,0.));
#8338=DIRECTION('',(0.,-1.,0.));
#8339=DIRECTION('center_axis',(0.707106781186548,0.707106781186548,0.));
#8340=DIRECTION('ref_axis',(-0.499999999999998,0.499999999999998,0.70710678118655));
#8341=DIRECTION('',(-0.707106781186548,-0.707106781186548,0.));
#8342=DIRECTION('',(0.707106781186548,0.707106781186548,0.));
#8343=DIRECTION('center_axis',(-0.923879532511286,-0.382683432365092,0.));
#8344=DIRECTION('ref_axis',(0.382683432365092,-0.923879532511286,0.));
#8345=DIRECTION('center_axis',(-1.,0.,0.));
#8346=DIRECTION('ref_axis',(0.,0.707106781186548,0.707106781186548));
#8347=DIRECTION('',(-1.,0.,0.));
#8348=DIRECTION('',(1.,0.,0.));
#8349=DIRECTION('center_axis',(-0.923879532511286,0.382683432365092,0.));
#8350=DIRECTION('ref_axis',(0.382683432365092,0.923879532511286,0.));
#8351=DIRECTION('center_axis',(0.707106781186548,-0.707106781186548,0.));
#8352=DIRECTION('ref_axis',(0.499999999999998,0.499999999999998,0.70710678118655));
#8353=DIRECTION('',(-0.707106781186548,0.707106781186548,0.));
#8354=DIRECTION('',(0.707106781186548,-0.707106781186548,0.));
#8355=DIRECTION('center_axis',(-0.382683432365092,0.923879532511286,0.));
#8356=DIRECTION('ref_axis',(-0.923879532511286,-0.382683432365092,0.));
#8357=DIRECTION('center_axis',(0.,1.,0.));
#8358=DIRECTION('ref_axis',(0.707106781186548,0.,0.707106781186548));
#8359=DIRECTION('',(0.,1.,0.));
#8360=DIRECTION('',(0.,-1.,0.));
#8361=DIRECTION('center_axis',(0.382683432365092,0.923879532511286,-4.10284931589584E-15));
#8362=DIRECTION('ref_axis',(0.923879532511286,-0.382683432365092,-9.90515446280885E-15));
#8363=DIRECTION('center_axis',(-0.707106781186548,-0.707106781186548,0.));
#8364=DIRECTION('ref_axis',(0.499999999999998,-0.499999999999998,0.70710678118655));
#8365=DIRECTION('',(0.707106781186548,0.707106781186548,0.));
#8366=DIRECTION('',(-0.707106781186548,-0.707106781186548,0.));
#8367=DIRECTION('center_axis',(0.923879532511287,0.38268343236509,0.));
#8368=DIRECTION('ref_axis',(-0.38268343236509,0.923879532511287,0.));
#8369=DIRECTION('center_axis',(1.,0.,0.));
#8370=DIRECTION('ref_axis',(0.,-0.707106781186551,0.707106781186544));
#8371=DIRECTION('',(-1.,0.,0.));
#8372=DIRECTION('center_axis',(0.923879532511288,0.382683432365087,5.80230514691306E-15));
#8373=DIRECTION('ref_axis',(-0.382683432365087,0.923879532511288,1.40080037787049E-14));
#8374=DIRECTION('center_axis',(-0.707106781186548,-0.707106781186548,0.));
#8375=DIRECTION('ref_axis',(0.499999999999998,-0.499999999999998,0.70710678118655));
#8376=DIRECTION('',(-0.707106781186548,-0.707106781186548,0.));
#8377=DIRECTION('center_axis',(0.707106781186548,0.707106781186548,0.));
#8378=DIRECTION('ref_axis',(0.,0.,-1.));
#8379=DIRECTION('',(0.,0.,1.));
#8380=DIRECTION('',(0.,0.,-1.));
#8381=DIRECTION('center_axis',(1.,0.,0.));
#8382=DIRECTION('ref_axis',(0.,1.,0.));
#8383=DIRECTION('',(0.,0.,1.));
#8384=DIRECTION('center_axis',(0.707106781186548,-0.707106781186548,0.));
#8385=DIRECTION('ref_axis',(0.,0.,-1.));
#8386=DIRECTION('center_axis',(0.,0.,1.));
#8387=DIRECTION('ref_axis',(1.,0.,0.));
#8388=DIRECTION('center_axis',(-0.707106781186548,0.707106781186548,0.));
#8389=DIRECTION('ref_axis',(0.,0.,1.));
#8390=DIRECTION('',(0.,0.,1.));
#8391=DIRECTION('',(0.,0.,-1.));
#8392=DIRECTION('center_axis',(0.,1.,0.));
#8393=DIRECTION('ref_axis',(-1.,0.,0.));
#8394=DIRECTION('center_axis',(-1.,0.,0.));
#8395=DIRECTION('ref_axis',(0.,-1.,0.));
#9927=CARTESIAN_POINT('',(0.,0.,0.));
#9928=CARTESIAN_POINT('Origin',(29.,-25.,36.));
#9929=CARTESIAN_POINT('',(30.,-35.,36.));
#9930=CARTESIAN_POINT('',(30.,-45.,36.));
#9931=CARTESIAN_POINT('',(30.,-25.,36.));
#9932=CARTESIAN_POINT('',(29.,-44.5857864376269,35.));
#9933=CARTESIAN_POINT('Origin',(29.,-44.5857864376269,36.));
#9934=CARTESIAN_POINT('',(29.,-34.5857864376269,35.));
#9935=CARTESIAN_POINT('',(29.,-25.,35.));
#9936=CARTESIAN_POINT('Origin',(29.,-34.5857864376269,36.));
#9937=CARTESIAN_POINT('Origin',(15.,-29.,36.));
#9938=CARTESIAN_POINT('',(34.5857864376269,-29.,35.));
#9939=CARTESIAN_POINT('',(44.5857864376269,-29.,35.));
#9940=CARTESIAN_POINT('',(15.,-29.,35.));
#9941=CARTESIAN_POINT('',(45.,-30.,36.));
#9942=CARTESIAN_POINT('Origin',(44.5857864376269,-29.,36.));
#9943=CARTESIAN_POINT('',(35.,-30.,36.));
#9944=CARTESIAN_POINT('',(15.,-30.,36.));
#9945=CARTESIAN_POINT('Origin',(34.5857864376269,-29.,36.));
#9946=CARTESIAN_POINT('Origin',(41.7928932188135,-31.7928932188135,36.));
#9947=CARTESIAN_POINT('',(49.,-24.5857864376269,35.));
#9948=CARTESIAN_POINT('',(41.7928932188135,-31.7928932188135,35.));
#9949=CARTESIAN_POINT('',(50.,-25.,36.));
#9950=CARTESIAN_POINT('Origin',(49.,-24.5857864376269,36.));
#9951=CARTESIAN_POINT('',(42.5,-32.5,36.));
#9952=CARTESIAN_POINT('Origin',(49.,-15.,36.));
#9953=CARTESIAN_POINT('',(49.,44.5857864376269,35.));
#9954=CARTESIAN_POINT('',(49.,-15.,35.));
#9955=CARTESIAN_POINT('',(50.,45.,36.));
#9956=CARTESIAN_POINT('Origin',(49.,44.5857864376269,36.));
#9957=CARTESIAN_POINT('',(50.,-15.,36.));
#9958=CARTESIAN_POINT('Origin',(46.7928932188135,46.7928932188135,36.));
#9959=CARTESIAN_POINT('',(44.5857864376269,49.,35.));
#9960=CARTESIAN_POINT('',(46.7928932188135,46.7928932188135,35.));
#9961=CARTESIAN_POINT('',(45.,50.,36.));
#9962=CARTESIAN_POINT('Origin',(44.5857864376269,49.,36.));
#9963=CARTESIAN_POINT('',(47.5,47.5,36.));
#9964=CARTESIAN_POINT('Origin',(25.,49.,36.));
#9965=CARTESIAN_POINT('',(-44.5857864376269,49.,35.));
#9966=CARTESIAN_POINT('',(25.,49.,35.));
#9967=CARTESIAN_POINT('',(-45.,50.,36.));
#9968=CARTESIAN_POINT('Origin',(-44.5857864376269,49.,36.));
#9969=CARTESIAN_POINT('',(25.,50.,36.));
#9970=CARTESIAN_POINT('Origin',(-46.7928932188135,46.7928932188135,36.));
#9971=CARTESIAN_POINT('',(-50.,45.,36.));
#9972=CARTESIAN_POINT('',(-47.5,47.5,36.));
#9973=CARTESIAN_POINT('',(-49.,44.5857864376269,35.));
#9974=CARTESIAN_POINT('',(-46.7928932188135,46.7928932188135,35.));
#9975=CARTESIAN_POINT('Origin',(-49.,44.5857864376269,36.));
#9976=CARTESIAN_POINT('Origin',(-49.,25.,36.));
#9977=CARTESIAN_POINT('',(-50.,-45.,36.));
#9978=CARTESIAN_POINT('',(-50.,25.,36.));
#9979=CARTESIAN_POINT('',(-49.,-44.5857864376269,35.));
#9980=CARTESIAN_POINT('',(-49.,25.,35.));
#9981=CARTESIAN_POINT('Origin',(-49.,-44.5857864376269,36.));
#9982=CARTESIAN_POINT('Origin',(-46.7928932188135,-46.7928932188135,36.));
#9983=CARTESIAN_POINT('',(-45.,-50.,36.));
#9984=CARTESIAN_POINT('',(-47.5,-47.5,36.));
#9985=CARTESIAN_POINT('',(-44.5857864376269,-49.,35.));
#9986=CARTESIAN_POINT('',(-46.7928932188135,-46.7928932188135,35.));
#9987=CARTESIAN_POINT('Origin',(-44.5857864376269,-49.,36.));
#9988=CARTESIAN_POINT('Origin',(-25.,-49.,36.));
#9989=CARTESIAN_POINT('',(25.,-50.,36.));
#9990=CARTESIAN_POINT('',(-25.,-50.,36.));
#9991=CARTESIAN_POINT('',(24.5857864376269,-49.,35.));
#9992=CARTESIAN_POINT('',(-25.,-49.,35.));
#9993=CARTESIAN_POINT('Origin',(24.5857864376269,-49.,36.));
#9994=CARTESIAN_POINT('Origin',(31.7928932188135,-41.7928932188135,36.));
#9995=CARTESIAN_POINT('',(32.5,-42.5,36.));
#9996=CARTESIAN_POINT('',(31.7928932188135,-41.7928932188135,35.));
#9997=CARTESIAN_POINT('Origin',(31.7928932188135,-31.7928932188135,36.));
#9998=CARTESIAN_POINT('',(32.5,-32.5,36.));
#9999=CARTESIAN_POINT('',(31.7928932188135,-31.7928932188135,35.));
#10000=CARTESIAN_POINT('Origin',(-47.5,-47.5,35.));
#10001=CARTESIAN_POINT('',(-45.,-50.,49.));
#10002=CARTESIAN_POINT('',(-45.,-50.,35.));
#10003=CARTESIAN_POINT('',(-50.,-45.,49.));
#10004=CARTESIAN_POINT('',(-47.5,-47.5,49.));
#10005=CARTESIAN_POINT('',(-50.,-45.,35.));
#10006=CARTESIAN_POINT('Origin',(-50.,-50.,35.));
#10007=CARTESIAN_POINT('',(25.,-50.,49.));
#10008=CARTESIAN_POINT('',(25.,-50.,35.));
#10009=CARTESIAN_POINT('',(-25.,-50.,49.));
#10010=CARTESIAN_POINT('Origin',(27.5,-47.5,35.));
#10011=CARTESIAN_POINT('',(30.,-45.,49.));
#10012=CARTESIAN_POINT('',(30.,-45.,35.));
#10013=CARTESIAN_POINT('',(32.5,-42.5,49.));
#10014=CARTESIAN_POINT('Origin',(30.,-50.,35.));
#10015=CARTESIAN_POINT('',(30.,-35.,49.));
#10016=CARTESIAN_POINT('',(30.,-35.,35.));
#10017=CARTESIAN_POINT('',(30.,-25.,49.));
#10018=CARTESIAN_POINT('Origin',(32.5,-32.5,35.));
#10019=CARTESIAN_POINT('',(35.,-30.,49.));
#10020=CARTESIAN_POINT('',(35.,-30.,35.));
#10021=CARTESIAN_POINT('',(32.5,-32.5,49.));
#10022=CARTESIAN_POINT('Origin',(30.,-30.,35.));
#10023=CARTESIAN_POINT('',(45.,-30.,49.));
#10024=CARTESIAN_POINT('',(45.,-30.,35.));
#10025=CARTESIAN_POINT('',(15.,-30.,49.));
#10026=CARTESIAN_POINT('Origin',(0.,0.,35.));
#10027=CARTESIAN_POINT('Origin',(29.,-25.,49.));
#10028=CARTESIAN_POINT('',(29.,-34.5857864376269,50.));
#10029=CARTESIAN_POINT('',(29.,-44.5857864376269,50.));
#10030=CARTESIAN_POINT('',(29.,-25.,50.));
#10031=CARTESIAN_POINT('Origin',(29.,-44.5857864376269,49.));
#10032=CARTESIAN_POINT('Origin',(29.,-34.5857864376269,49.));
#10033=CARTESIAN_POINT('Origin',(31.7928932188135,-41.7928932188135,49.));
#10034=CARTESIAN_POINT('',(24.5857864376269,-49.,50.));
#10035=CARTESIAN_POINT('',(31.7928932188135,-41.7928932188135,50.));
#10036=CARTESIAN_POINT('Origin',(24.5857864376269,-49.,49.));
#10037=CARTESIAN_POINT('Origin',(-25.,-49.,49.));
#10038=CARTESIAN_POINT('',(-44.5857864376269,-49.,50.));
#10039=CARTESIAN_POINT('',(-25.,-49.,50.));
#10040=CARTESIAN_POINT('Origin',(-44.5857864376269,-49.,49.));
#10041=CARTESIAN_POINT('Origin',(-46.7928932188135,-46.7928932188135,49.));
#10042=CARTESIAN_POINT('',(-49.,-44.5857864376269,50.));
#10043=CARTESIAN_POINT('',(-46.7928932188135,-46.7928932188135,50.));
#10044=CARTESIAN_POINT('Origin',(-49.,-44.5857864376269,49.));
#10045=CARTESIAN_POINT('Origin',(-49.,25.,49.));
#10046=CARTESIAN_POINT('',(-49.,44.5857864376269,50.));
#10047=CARTESIAN_POINT('',(-49.,25.,50.));
#10048=CARTESIAN_POINT('',(-50.,45.,49.));
#10049=CARTESIAN_POINT('Origin',(-49.,44.5857864376269,49.));
#10050=CARTESIAN_POINT('',(-50.,25.,49.));
#10051=CARTESIAN_POINT('Origin',(-46.7928932188135,46.7928932188135,49.));
#10052=CARTESIAN_POINT('',(-45.,50.,49.));
#10053=CARTESIAN_POINT('',(-47.5,47.5,49.));
#10054=CARTESIAN_POINT('',(-44.5857864376269,49.,50.));
#10055=CARTESIAN_POINT('',(-46.7928932188135,46.7928932188135,50.));
#10056=CARTESIAN_POINT('Origin',(-44.5857864376269,49.,49.));
#10057=CARTESIAN_POINT('Origin',(25.,49.,49.));
#10058=CARTESIAN_POINT('',(45.,50.,49.));
#10059=CARTESIAN_POINT('',(25.,50.,49.));
#10060=CARTESIAN_POINT('',(44.5857864376269,49.,50.));
#10061=CARTESIAN_POINT('',(25.,49.,50.));
#10062=CARTESIAN_POINT('Origin',(44.5857864376269,49.,49.));
#10063=CARTESIAN_POINT('Origin',(46.7928932188135,46.7928932188135,49.));
#10064=CARTESIAN_POINT('',(50.,45.,49.));
#10065=CARTESIAN_POINT('',(47.5,47.5,49.));
#10066=CARTESIAN_POINT('',(49.,44.5857864376269,50.));
#10067=CARTESIAN_POINT('',(46.7928932188135,46.7928932188135,50.));
#10068=CARTESIAN_POINT('Origin',(49.,44.5857864376269,49.));
#10069=CARTESIAN_POINT('Origin',(49.,-15.,49.));
#10070=CARTESIAN_POINT('',(50.,-25.,49.));
#10071=CARTESIAN_POINT('',(50.,-15.,49.));
#10072=CARTESIAN_POINT('',(49.,-24.5857864376269,50.));
#10073=CARTESIAN_POINT('',(49.,-15.,50.));
#10074=CARTESIAN_POINT('Origin',(49.,-24.5857864376269,49.));
#10075=CARTESIAN_POINT('Origin',(41.7928932188135,-31.7928932188135,49.));
#10076=CARTESIAN_POINT('',(42.5,-32.5,49.));
#10077=CARTESIAN_POINT('',(44.5857864376269,-29.,50.));
#10078=CARTESIAN_POINT('',(41.7928932188135,-31.7928932188135,50.));
#10079=CARTESIAN_POINT('Origin',(44.5857864376269,-29.,49.));
#10080=CARTESIAN_POINT('Origin',(15.,-29.,49.));
#10081=CARTESIAN_POINT('',(34.5857864376269,-29.,50.));
#10082=CARTESIAN_POINT('',(15.,-29.,50.));
#10083=CARTESIAN_POINT('Origin',(34.5857864376269,-29.,49.));
#10084=CARTESIAN_POINT('Origin',(31.7928932188135,-31.7928932188135,49.));
#10085=CARTESIAN_POINT('',(31.7928932188135,-31.7928932188135,50.));
#10086=CARTESIAN_POINT('Origin',(47.5,47.5,35.));
#10087=CARTESIAN_POINT('',(45.,50.,35.));
#10088=CARTESIAN_POINT('',(50.,45.,35.));
#10089=CARTESIAN_POINT('Origin',(50.,-30.,35.));
#10090=CARTESIAN_POINT('',(50.,-25.,35.));
#10091=CARTESIAN_POINT('Origin',(47.5,-27.5,35.));
#10092=CARTESIAN_POINT('Origin',(0.,0.,50.));
#10093=CARTESIAN_POINT('Origin',(-47.5,47.5,35.));
#10094=CARTESIAN_POINT('',(-50.,45.,35.));
#10095=CARTESIAN_POINT('',(-45.,50.,35.));
#10096=CARTESIAN_POINT('Origin',(50.,50.,35.));
#10097=CARTESIAN_POINT('Origin',(-50.,50.,35.));
#10118=UNCERTAINTY_MEASURE_WITH_UNIT(LENGTH_MEASURE(0.01),#10132,
'DISTANCE_ACCURACY_VALUE',
'Maximum model space distance between geometric entities at asserted c
onnectivities');
#10119=UNCERTAINTY_MEASURE_WITH_UNIT(LENGTH_MEASURE(0.01),#10132,
'DISTANCE_ACCURACY_VALUE',
'Maximum model space distance between geometric entities at asserted c
onnectivities');
#10130=(
GEOMETRIC_REPRESENTATION_CONTEXT(3)
GLOBAL_UNCERTAINTY_ASSIGNED_CONTEXT((#10118))
GLOBAL_UNIT_ASSIGNED_CONTEXT((#10132,#10134,#10135))
REPRESENTATION_CONTEXT('','3D')
);
#10131=(
GEOMETRIC_REPRESENTATION_CONTEXT(3)
GLOBAL_UNCERTAINTY_ASSIGNED_CONTEXT((#10119))
GLOBAL_UNIT_ASSIGNED_CONTEXT((#10132,#10134,#10135))
REPRESENTATION_CONTEXT('','3D')
);
#10132=(
LENGTH_UNIT()
NAMED_UNIT(*)
SI_UNIT(.MILLI.,.METRE.)
);
#10134=(
NAMED_UNIT(*)
PLANE_ANGLE_UNIT()
SI_UNIT($,.RADIAN.)
);
#10135=(
NAMED_UNIT(*)
SI_UNIT($,.STERADIAN.)
SOLID_ANGLE_UNIT()
);
#10146=SHAPE_DEFINITION_REPRESENTATION(#10157,#10178);
#10157=PRODUCT_DEFINITION_SHAPE('',$,#10190);
#10178=SHAPE_REPRESENTATION('',(#6549),#10130);
#10179=PRODUCT_DEFINITION_CONTEXT('part definition',#10214,'design');
#10190=PRODUCT_DEFINITION('Bottom_Block_02','Bottom_Block_02',#10201,#10179);
#10201=PRODUCT_DEFINITION_FORMATION('',$,#10226);
#10214=APPLICATION_CONTEXT(
'Core Data for Automotive Mechanical Design Process');
#10215=PRODUCT_CONTEXT('part definition',#10214,'mechanical');
#10226=PRODUCT('Bottom_Block_02','Bottom_Block_02',$,(#10215));
#10241=COLOUR_RGB('Dark Blue',0.08,0.2,0.34);
#10242=FILL_AREA_STYLE_COLOUR('',#10241);
#10243=FILL_AREA_STYLE('',(#10242));
#10244=SURFACE_STYLE_FILL_AREA(#10243);
#10245=SURFACE_SIDE_STYLE('',(#10244));
#10246=SURFACE_STYLE_USAGE(.BOTH.,#10245);
#10247=PRESENTATION_STYLE_ASSIGNMENT((#10246));
ENDSEC;
END-ISO-10303-21;
